ISO-10303-21;
HEADER;
/* Generated by software containing ST-Developer
 * from STEP Tools, Inc. (www.steptools.com) 
 */

FILE_DESCRIPTION(
/* description */ ('Bin tilter linkage'),
/* implementation_level */ '2;1');

FILE_NAME(
/* name */ 'M4 short cap screw.step',
/* time_stamp */ '2026-10-28T03:26:24-07:00',
/* author */ (''),
/* organization */ (''),
/* preprocessor_version */ 'ST-DEVELOPER v20.2',
/* originating_system */ 'Autodesk Translation Framework v15.17.0.0',
/* authorisation */ '');

FILE_SCHEMA (('AUTOMOTIVE_DESIGN { 1 0 10303 214 3 1 1 }'));
ENDSEC;

DATA;
#10=MECHANICAL_DESIGN_GEOMETRIC_PRESENTATION_REPRESENTATION('',(#894),#23728);
#682=SHAPE_REPRESENTATION_RELATIONSHIP('SRR','None',#24147,#788);
#788=ADVANCED_BREP_SHAPE_REPRESENTATION('',(#1007),#23647);
#894=STYLED_ITEM('',(#24772),#1007);
#1007=MANIFOLD_SOLID_BREP('Body1',#12425);
#1264=FACE_BOUND('',#3118,.T.);
#1623=PLANE('',#14265);
#1624=PLANE('',#14270);
#1625=PLANE('',#14273);
#2163=FACE_OUTER_BOUND('',#3117,.T.);
#2164=FACE_OUTER_BOUND('',#3119,.T.);
#2165=FACE_OUTER_BOUND('',#3120,.T.);
#2166=FACE_OUTER_BOUND('',#3121,.T.);
#2167=FACE_OUTER_BOUND('',#3122,.T.);
#3117=EDGE_LOOP('',(#9493));
#3118=EDGE_LOOP('',(#9494));
#3119=EDGE_LOOP('',(#9495,#9496,#9497,#9498));
#3120=EDGE_LOOP('',(#9499));
#3121=EDGE_LOOP('',(#9500,#9501,#9502,#9503));
#3122=EDGE_LOOP('',(#9504));
#4129=LINE('',#20993,#4804);
#4130=LINE('',#20999,#4805);
#4804=VECTOR('',#16940,0.35);
#4805=VECTOR('',#16949,0.2);
#5479=CIRCLE('',#14266,0.35);
#5480=CIRCLE('',#14267,0.2);
#5481=CIRCLE('',#14269,0.35);
#5482=CIRCLE('',#14272,0.2);
#6329=VERTEX_POINT('',#20987);
#6330=VERTEX_POINT('',#20989);
#6331=VERTEX_POINT('',#20992);
#6332=VERTEX_POINT('',#20997);
#7486=EDGE_CURVE('',#6329,#6329,#5479,.T.);
#7487=EDGE_CURVE('',#6330,#6330,#5480,.T.);
#7488=EDGE_CURVE('',#6329,#6331,#4129,.T.);
#7489=EDGE_CURVE('',#6331,#6331,#5481,.T.);
#7490=EDGE_CURVE('',#6332,#6332,#5482,.T.);
#7491=EDGE_CURVE('',#6332,#6330,#4130,.T.);
#9493=ORIENTED_EDGE('',*,*,#7486,.T.);
#9494=ORIENTED_EDGE('',*,*,#7487,.F.);
#9495=ORIENTED_EDGE('',*,*,#7486,.F.);
#9496=ORIENTED_EDGE('',*,*,#7488,.T.);
#9497=ORIENTED_EDGE('',*,*,#7489,.T.);
#9498=ORIENTED_EDGE('',*,*,#7488,.F.);
#9499=ORIENTED_EDGE('',*,*,#7489,.F.);
#9500=ORIENTED_EDGE('',*,*,#7490,.F.);
#9501=ORIENTED_EDGE('',*,*,#7491,.T.);
#9502=ORIENTED_EDGE('',*,*,#7487,.T.);
#9503=ORIENTED_EDGE('',*,*,#7491,.F.);
#9504=ORIENTED_EDGE('',*,*,#7490,.T.);
#11405=CYLINDRICAL_SURFACE('',#14268,0.35);
#11406=CYLINDRICAL_SURFACE('',#14271,0.2);
#11888=ADVANCED_FACE('',(#2163,#1264),#1623,.T.);
#11889=ADVANCED_FACE('',(#2164),#11405,.T.);
#11890=ADVANCED_FACE('',(#2165),#1624,.F.);
#11891=ADVANCED_FACE('',(#2166),#11406,.T.);
#11892=ADVANCED_FACE('',(#2167),#1625,.T.);
#12425=CLOSED_SHELL('',(#11888,#11889,#11890,#11891,#11892));
#14264=AXIS2_PLACEMENT_3D('',#20985,#16930,#16931);
#14265=AXIS2_PLACEMENT_3D('',#20986,#16932,#16933);
#14266=AXIS2_PLACEMENT_3D('',#20988,#16934,#16935);
#14267=AXIS2_PLACEMENT_3D('',#20990,#16936,#16937);
#14268=AXIS2_PLACEMENT_3D('',#20991,#16938,#16939);
#14269=AXIS2_PLACEMENT_3D('',#20994,#16941,#16942);
#14270=AXIS2_PLACEMENT_3D('',#20995,#16943,#16944);
#14271=AXIS2_PLACEMENT_3D('',#20996,#16945,#16946);
#14272=AXIS2_PLACEMENT_3D('',#20998,#16947,#16948);
#14273=AXIS2_PLACEMENT_3D('',#21000,#16950,#16951);
#16930=DIRECTION('axis',(0.,0.,1.));
#16931=DIRECTION('refdir',(1.,0.,0.));
#16932=DIRECTION('center_axis',(0.,1.,0.));
#16933=DIRECTION('ref_axis',(1.,0.,0.));
#16934=DIRECTION('center_axis',(0.,1.,0.));
#16935=DIRECTION('ref_axis',(1.,0.,0.));
#16936=DIRECTION('center_axis',(0.,1.,0.));
#16937=DIRECTION('ref_axis',(1.,0.,0.));
#16938=DIRECTION('center_axis',(0.,1.,0.));
#16939=DIRECTION('ref_axis',(1.,0.,0.));
#16940=DIRECTION('',(0.,-1.,0.));
#16941=DIRECTION('center_axis',(0.,1.,0.));
#16942=DIRECTION('ref_axis',(1.,0.,0.));
#16943=DIRECTION('center_axis',(0.,1.,0.));
#16944=DIRECTION('ref_axis',(1.,0.,0.));
#16945=DIRECTION('center_axis',(0.,1.,0.));
#16946=DIRECTION('ref_axis',(1.,0.,0.));
#16947=DIRECTION('center_axis',(0.,1.,0.));
#16948=DIRECTION('ref_axis',(1.,0.,0.));
#16949=DIRECTION('',(0.,-1.,0.));
#16950=DIRECTION('center_axis',(0.,1.,0.));
#16951=DIRECTION('ref_axis',(1.,0.,0.));
#20985=CARTESIAN_POINT('',(0.,0.,0.));
#20986=CARTESIAN_POINT('Origin',(1.30814754519511,-0.8,16.3081475451951));
#20987=CARTESIAN_POINT('',(0.958147545195113,-0.8,16.3081475451951));
#20988=CARTESIAN_POINT('Origin',(1.30814754519511,-0.8,16.3081475451951));
#20989=CARTESIAN_POINT('',(1.10814754519511,-0.8,16.3081475451951));
#20990=CARTESIAN_POINT('Origin',(1.30814754519511,-0.8,16.3081475451951));
#20991=CARTESIAN_POINT('Origin',(1.30814754519511,-1.2,16.3081475451951));
#20992=CARTESIAN_POINT('',(0.958147545195113,-1.2,16.3081475451951));
#20993=CARTESIAN_POINT('',(0.958147545195113,-1.2,16.3081475451951));
#20994=CARTESIAN_POINT('Origin',(1.30814754519511,-1.2,16.3081475451951));
#20995=CARTESIAN_POINT('Origin',(1.30814754519511,-1.2,16.3081475451951));
#20996=CARTESIAN_POINT('Origin',(1.30814754519511,-0.8,16.3081475451951));
#20997=CARTESIAN_POINT('',(1.10814754519511,-0.1,16.3081475451951));
#20998=CARTESIAN_POINT('Origin',(1.30814754519511,-0.1,16.3081475451951));
#20999=CARTESIAN_POINT('',(1.10814754519511,-0.8,16.3081475451951));
#21000=CARTESIAN_POINT('Origin',(1.30814754519511,-0.1,16.3081475451951));
#23530=UNCERTAINTY_MEASURE_WITH_UNIT(LENGTH_MEASURE(0.001),#23729,
'DISTANCE_ACCURACY_VALUE',
'Maximum model space distance between geometric entities at asserted c
onnectivities');
#23611=UNCERTAINTY_MEASURE_WITH_UNIT(LENGTH_MEASURE(0.001),#23729,
'DISTANCE_ACCURACY_VALUE',
'Maximum model space distance between geometric entities at asserted c
onnectivities');
#23647=(
GEOMETRIC_REPRESENTATION_CONTEXT(3)
GLOBAL_UNCERTAINTY_ASSIGNED_CONTEXT((#23530))
GLOBAL_UNIT_ASSIGNED_CONTEXT((#23729,#23731,#23732))
REPRESENTATION_CONTEXT('','3D')
);
#23728=(
GEOMETRIC_REPRESENTATION_CONTEXT(3)
GLOBAL_UNCERTAINTY_ASSIGNED_CONTEXT((#23611))
GLOBAL_UNIT_ASSIGNED_CONTEXT((#23729,#23731,#23732))
REPRESENTATION_CONTEXT('','3D')
);
#23729=(
LENGTH_UNIT()
NAMED_UNIT(*)
SI_UNIT(.CENTI.,.METRE.)
);
#23731=(
NAMED_UNIT(*)
PLANE_ANGLE_UNIT()
SI_UNIT($,.RADIAN.)
);
#23732=(
NAMED_UNIT(*)
SI_UNIT($,.STERADIAN.)
SOLID_ANGLE_UNIT()
);
#23768=SHAPE_DEFINITION_REPRESENTATION(#23884,#24147);
#23884=PRODUCT_DEFINITION_SHAPE('',$,#24264);
#24147=SHAPE_REPRESENTATION('',(#14264),#23647);
#24228=PRODUCT_DEFINITION_CONTEXT('part definition',#24578,'design');
#24264=PRODUCT_DEFINITION('M4 short cap screw','M4 short cap screw',#24380,
#24228);
#24380=PRODUCT_DEFINITION_FORMATION('',$,#24615);
#24578=APPLICATION_CONTEXT(
'Core Data for Automotive Mechanical Design Process');
#24579=PRODUCT_CONTEXT('part definition',#24578,'mechanical');
#24615=PRODUCT('M4 short cap screw','M4 short cap screw',
'M4 short cap screw',(#24579));
#24766=COLOUR_RGB('Black',0.12,0.14,0.17);
#24767=FILL_AREA_STYLE_COLOUR('',#24766);
#24768=FILL_AREA_STYLE('',(#24767));
#24769=SURFACE_STYLE_FILL_AREA(#24768);
#24770=SURFACE_SIDE_STYLE('',(#24769));
#24771=SURFACE_STYLE_USAGE(.BOTH.,#24770);
#24772=PRESENTATION_STYLE_ASSIGNMENT((#24771));
ENDSEC;
END-ISO-10303-21;
